ISO-10303-21;
HEADER;
/* Generated by software containing ST-Developer
 * from STEP Tools, Inc. (www.steptools.com) 
 */

FILE_DESCRIPTION(
/* description */ ('Ball-race swivel caster'),
/* implementation_level */ '2;1');

FILE_NAME(
/* name */ 'Flat Washer - M8.step',
/* time_stamp */ '2026-10-29T16:15:51-07:00',
/* author */ (''),
/* organization */ (''),
/* preprocessor_version */ 'ST-DEVELOPER v20.2',
/* originating_system */ 'Autodesk Translation Framework v15.17.0.0',
/* authorisation */ '');

FILE_SCHEMA (('AUTOMOTIVE_DESIGN { 1 0 10303 214 3 1 1 }'));
ENDSEC;

DATA;
#10=MECHANICAL_DESIGN_GEOMETRIC_PRESENTATION_REPRESENTATION('',(#312),#7816);
#263=SHAPE_REPRESENTATION_RELATIONSHIP('SRR','None',#7909,#283);
#283=ADVANCED_BREP_SHAPE_REPRESENTATION('',(#348),#7798);
#312=STYLED_ITEM('',(#8104),#348);
#348=MANIFOLD_SOLID_BREP('Body1',#3718);
#408=FACE_BOUND('',#855,.T.);
#409=FACE_BOUND('',#857,.T.);
#455=PLANE('',#4204);
#456=PLANE('',#4205);
#604=FACE_OUTER_BOUND('',#852,.T.);
#605=FACE_OUTER_BOUND('',#853,.T.);
#606=FACE_OUTER_BOUND('',#854,.T.);
#607=FACE_OUTER_BOUND('',#856,.T.);
#852=EDGE_LOOP('',(#2915,#2916,#2917,#2918));
#853=EDGE_LOOP('',(#2919,#2920,#2921,#2922));
#854=EDGE_LOOP('',(#2923));
#855=EDGE_LOOP('',(#2924));
#856=EDGE_LOOP('',(#2925));
#857=EDGE_LOOP('',(#2926));
#1056=LINE('',#6845,#1211);
#1057=LINE('',#6851,#1212);
#1211=VECTOR('',#5010,0.42);
#1212=VECTOR('',#5017,0.8);
#1465=CIRCLE('',#4199,0.42);
#1466=CIRCLE('',#4200,0.42);
#1467=CIRCLE('',#4202,0.8);
#1468=CIRCLE('',#4203,0.8);
#1759=VERTEX_POINT('',#6842);
#1760=VERTEX_POINT('',#6844);
#1761=VERTEX_POINT('',#6848);
#1762=VERTEX_POINT('',#6850);
#2177=EDGE_CURVE('',#1759,#1759,#1465,.T.);
#2178=EDGE_CURVE('',#1759,#1760,#1056,.T.);
#2179=EDGE_CURVE('',#1760,#1760,#1466,.T.);
#2180=EDGE_CURVE('',#1761,#1761,#1467,.T.);
#2181=EDGE_CURVE('',#1761,#1762,#1057,.T.);
#2182=EDGE_CURVE('',#1762,#1762,#1468,.T.);
#2915=ORIENTED_EDGE('',*,*,#2177,.F.);
#2916=ORIENTED_EDGE('',*,*,#2178,.T.);
#2917=ORIENTED_EDGE('',*,*,#2179,.T.);
#2918=ORIENTED_EDGE('',*,*,#2178,.F.);
#2919=ORIENTED_EDGE('',*,*,#2180,.F.);
#2920=ORIENTED_EDGE('',*,*,#2181,.T.);
#2921=ORIENTED_EDGE('',*,*,#2182,.T.);
#2922=ORIENTED_EDGE('',*,*,#2181,.F.);
#2923=ORIENTED_EDGE('',*,*,#2180,.T.);
#2924=ORIENTED_EDGE('',*,*,#2177,.T.);
#2925=ORIENTED_EDGE('',*,*,#2182,.F.);
#2926=ORIENTED_EDGE('',*,*,#2179,.F.);
#3460=CYLINDRICAL_SURFACE('',#4198,0.42);
#3461=CYLINDRICAL_SURFACE('',#4201,0.8);
#3575=ADVANCED_FACE('',(#604),#3460,.F.);
#3576=ADVANCED_FACE('',(#605),#3461,.T.);
#3577=ADVANCED_FACE('',(#606,#408),#455,.T.);
#3578=ADVANCED_FACE('',(#607,#409),#456,.F.);
#3718=CLOSED_SHELL('',(#3575,#3576,#3577,#3578));
#4197=AXIS2_PLACEMENT_3D('',#6840,#5004,#5005);
#4198=AXIS2_PLACEMENT_3D('',#6841,#5006,#5007);
#4199=AXIS2_PLACEMENT_3D('',#6843,#5008,#5009);
#4200=AXIS2_PLACEMENT_3D('',#6846,#5011,#5012);
#4201=AXIS2_PLACEMENT_3D('',#6847,#5013,#5014);
#4202=AXIS2_PLACEMENT_3D('',#6849,#5015,#5016);
#4203=AXIS2_PLACEMENT_3D('',#6852,#5018,#5019);
#4204=AXIS2_PLACEMENT_3D('',#6853,#5020,#5021);
#4205=AXIS2_PLACEMENT_3D('',#6854,#5022,#5023);
#5004=DIRECTION('axis',(0.,0.,1.));
#5005=DIRECTION('refdir',(1.,0.,0.));
#5006=DIRECTION('center_axis',(0.,1.,0.));
#5007=DIRECTION('ref_axis',(1.,0.,0.));
#5008=DIRECTION('center_axis',(0.,-1.,0.));
#5009=DIRECTION('ref_axis',(1.,0.,0.));
#5010=DIRECTION('',(0.,-1.,0.));
#5011=DIRECTION('center_axis',(0.,-1.,0.));
#5012=DIRECTION('ref_axis',(1.,0.,0.));
#5013=DIRECTION('center_axis',(0.,1.,0.));
#5014=DIRECTION('ref_axis',(1.,0.,0.));
#5015=DIRECTION('center_axis',(0.,1.,0.));
#5016=DIRECTION('ref_axis',(1.,0.,0.));
#5017=DIRECTION('',(0.,-1.,0.));
#5018=DIRECTION('center_axis',(0.,1.,0.));
#5019=DIRECTION('ref_axis',(1.,0.,0.));
#5020=DIRECTION('center_axis',(0.,1.,0.));
#5021=DIRECTION('ref_axis',(1.,0.,0.));
#5022=DIRECTION('center_axis',(0.,1.,0.));
#5023=DIRECTION('ref_axis',(1.,0.,0.));
#6840=CARTESIAN_POINT('',(0.,0.,0.));
#6841=CARTESIAN_POINT('Origin',(0.,0.,0.));
#6842=CARTESIAN_POINT('',(-0.42,0.16,5.14351655641888E-17));
#6843=CARTESIAN_POINT('Origin',(0.,0.16,0.));
#6844=CARTESIAN_POINT('',(-0.42,0.,5.14351655641888E-17));
#6845=CARTESIAN_POINT('',(-0.42,0.,5.14351655641888E-17));
#6846=CARTESIAN_POINT('Origin',(0.,0.,0.));
#6847=CARTESIAN_POINT('Origin',(0.,0.,0.));
#6848=CARTESIAN_POINT('',(-0.8,0.16,9.79717439317883E-17));
#6849=CARTESIAN_POINT('Origin',(0.,0.16,0.));
#6850=CARTESIAN_POINT('',(-0.8,0.,9.79717439317883E-17));
#6851=CARTESIAN_POINT('',(-0.8,0.,9.79717439317883E-17));
#6852=CARTESIAN_POINT('Origin',(0.,0.,0.));
#6853=CARTESIAN_POINT('Origin',(0.,0.16,0.));
#6854=CARTESIAN_POINT('Origin',(0.,0.,0.));
#7771=UNCERTAINTY_MEASURE_WITH_UNIT(LENGTH_MEASURE(0.001),#7817,
'DISTANCE_ACCURACY_VALUE',
'Maximum model space distance between geometric entities at asserted c
onnectivities');
#7789=UNCERTAINTY_MEASURE_WITH_UNIT(LENGTH_MEASURE(0.001),#7817,
'DISTANCE_ACCURACY_VALUE',
'Maximum model space distance between geometric entities at asserted c
onnectivities');
#7798=(
GEOMETRIC_REPRESENTATION_CONTEXT(3)
GLOBAL_UNCERTAINTY_ASSIGNED_CONTEXT((#7771))
GLOBAL_UNIT_ASSIGNED_CONTEXT((#7817,#7819,#7820))
REPRESENTATION_CONTEXT('','3D')
);
#7816=(
GEOMETRIC_REPRESENTATION_CONTEXT(3)
GLOBAL_UNCERTAINTY_ASSIGNED_CONTEXT((#7789))
GLOBAL_UNIT_ASSIGNED_CONTEXT((#7817,#7819,#7820))
REPRESENTATION_CONTEXT('','3D')
);
#7817=(
LENGTH_UNIT()
NAMED_UNIT(*)
SI_UNIT(.CENTI.,.METRE.)
);
#7819=(
NAMED_UNIT(*)
PLANE_ANGLE_UNIT()
SI_UNIT($,.RADIAN.)
);
#7820=(
NAMED_UNIT(*)
SI_UNIT($,.STERADIAN.)
SOLID_ANGLE_UNIT()
);
#7829=SHAPE_DEFINITION_REPRESENTATION(#7858,#7909);
#7858=PRODUCT_DEFINITION_SHAPE('',$,#7936);
#7909=SHAPE_REPRESENTATION('',(#4197),#7798);
#7927=PRODUCT_DEFINITION_CONTEXT('part definition',#8007,'design');
#7936=PRODUCT_DEFINITION('Flat Washer - M8','Flat Washer - M8',#7962,#7927);
#7962=PRODUCT_DEFINITION_FORMATION('',$,#8017);
#8007=APPLICATION_CONTEXT(
'Core Data for Automotive Mechanical Design Process');
#8008=PRODUCT_CONTEXT('part definition',#8007,'mechanical');
#8017=PRODUCT('Flat Washer - M8','Flat Washer - M8','Flat Washer - M8',
(#8008));
#8098=COLOUR_RGB('Black',0.12,0.14,0.17);
#8099=FILL_AREA_STYLE_COLOUR('',#8098);
#8100=FILL_AREA_STYLE('',(#8099));
#8101=SURFACE_STYLE_FILL_AREA(#8100);
#8102=SURFACE_SIDE_STYLE('',(#8101));
#8103=SURFACE_STYLE_USAGE(.BOTH.,#8102);
#8104=PRESENTATION_STYLE_ASSIGNMENT((#8103));
ENDSEC;
END-ISO-10303-21;
